ISO-10303-21;
HEADER;
FILE_DESCRIPTION (('STEP AP214'),
    '1' );
FILE_NAME ('Hinge Pin.step',
    '2026-10-06T08:24:18',
    ( '' ),
    ( '' ),
    'SwSTEP 2.0',
    'SolidWorks 2020',
    '' );
FILE_SCHEMA (( 'AUTOMOTIVE_DESIGN' ));
ENDSEC;

DATA;
#14=APPLICATION_CONTEXT ( 'automotive_design' ) ;
#54=ORIENTED_EDGE ( 'NONE', *, *, #9742, .F. ) ;
#101=ADVANCED_FACE ( 'NONE', ( #5000 ), #2827, .T. ) ;
#126=FACE_OUTER_BOUND ( 'NONE', #6487, .T. ) ;
#225=CARTESIAN_POINT ( 'NONE',  ( -72.90663470102438737, -12.40000000000001101, -371.7168990826883714 ) ) ;
#256=AXIS2_PLACEMENT_3D ( 'NONE', #918, #8989, #8337 ) ;
#333=DIRECTION ( 'NONE',  ( 0.000000000000000000, -1.000000000000000000, 0.000000000000000000 ) ) ;
#352=DIRECTION ( 'NONE',  ( 0.000000000000000000, -1.000000000000000000, 0.000000000000000000 ) ) ;
#353=ADVANCED_FACE ( 'NONE', ( #5555 ), #5229, .T. ) ;
#430=( NAMED_UNIT ( * ) PLANE_ANGLE_UNIT ( ) SI_UNIT ( $, .RADIAN. ) );
#491=ORIENTED_EDGE ( 'NONE', *, *, #8849, .T. ) ;
#524=DIRECTION ( 'NONE',  ( 0.000000000000000000, 0.000000000000000000, -1.000000000000000000 ) ) ;
#593=ORIENTED_EDGE ( 'NONE', *, *, #693, .T. ) ;
#603=AXIS2_PLACEMENT_3D ( 'NONE', #7287, #4114, #782 ) ;
#693=EDGE_CURVE ( 'NONE', #3804, #8252, #9594, .T. ) ;
#782=DIRECTION ( 'NONE',  ( 0.000000000000000000, 0.000000000000000000, -1.000000000000000000 ) ) ;
#813=DIRECTION ( 'NONE',  ( 0.000000000000000000, 0.000000000000000000, 1.000000000000000000 ) ) ;
#861=DIRECTION ( 'NONE',  ( 0.000000000000000000, 1.000000000000000000, 0.000000000000000000 ) ) ;
#873=ORIENTED_EDGE ( 'NONE', *, *, #6547, .F. ) ;
#914=MECHANICAL_DESIGN_GEOMETRIC_PRESENTATION_REPRESENTATION('',(#6938),#7105);
#918=CARTESIAN_POINT ( 'NONE',  ( -72.90663470102438737, -2.500000000000000444, -371.7168990826883714 ) ) ;
#920=CARTESIAN_POINT ( 'NONE',  ( -72.90663470102438737, -12.50000000000000000, -371.7168990826883714 ) ) ;
#985=ORIENTED_EDGE ( 'NONE', *, *, #6547, .T. ) ;
#1205=VERTEX_POINT ( 'NONE', #3453 ) ;
#1252=EDGE_CURVE ( 'NONE', #6040, #2579, #3555, .T. ) ;
#1256=CIRCLE ( 'NONE', #6764, 3.500000000000003109 ) ;
#1292=ORIENTED_EDGE ( 'NONE', *, *, #10149, .T. ) ;
#1369=CIRCLE ( 'NONE', #3267, 3.400000000000014122 ) ;
#1379=CIRCLE ( 'NONE', #9619, 3.400000000000014122 ) ;
#1498=SURFACE_SIDE_STYLE ('',( #5574 ) ) ;
#1505=CARTESIAN_POINT ( 'NONE',  ( -72.90663470102438737, 7.399494936611693774, -371.7168990826883714 ) ) ;
#1605=LINE ( 'NONE', #4877, #3330 ) ;
#1609=( NAMED_UNIT ( * ) SI_UNIT ( $, .STERADIAN. ) SOLID_ANGLE_UNIT ( ) );
#1618=AXIS2_PLACEMENT_3D ( 'NONE', #2125, #4595, #5289 ) ;
#1657=( LENGTH_UNIT ( ) NAMED_UNIT ( * ) SI_UNIT ( .MILLI., .METRE. ) );
#1664=DIRECTION ( 'NONE',  ( 0.000000000000000000, -0.7071067811864661934, -0.7071067811866287300 ) ) ;
#1666=AXIS2_PLACEMENT_3D ( 'NONE', #10062, #333, #3610 ) ;
#1675=CARTESIAN_POINT ( 'NONE',  ( -72.90663470102438737, -12.50000000000000000, -371.7168990826883714 ) ) ;
#1715=LINE ( 'NONE', #4987, #9837 ) ;
#1812=ADVANCED_FACE ( 'NONE', ( #5643 ), #8755, .T. ) ;
#1836=ORIENTED_EDGE ( 'NONE', *, *, #7471, .T. ) ;
#1844=UNCERTAINTY_MEASURE_WITH_UNIT (LENGTH_MEASURE( 1.000000000000000082E-05 ), #3000, 'distance_accuracy_value', 'NONE');
#1857=FACE_OUTER_BOUND ( 'NONE', #1966, .T. ) ;
#1910=PLANE ( 'NONE',  #9008 ) ;
#1966=EDGE_LOOP ( 'NONE', ( #6027, #7387 ) ) ;
#1994=SURFACE_STYLE_USAGE ( .BOTH. , #6281 ) ;
#2018=CARTESIAN_POINT ( 'NONE',  ( -72.90663470102438737, 7.399494936611693774, -368.2168990826883146 ) ) ;
#2043=PRESENTATION_STYLE_ASSIGNMENT (( #1994 ) ) ;
#2066=ORIENTED_EDGE ( 'NONE', *, *, #10269, .T. ) ;
#2088=VECTOR ( 'NONE', #1664, 1000.000000000000114 ) ;
#2125=CARTESIAN_POINT ( 'NONE',  ( -72.90663470102438737, 7.399494936611693774, -371.7168990826883714 ) ) ;
#2153=APPLICATION_CONTEXT ( 'automotive_design' ) ;
#2183=PRODUCT ( 'Hinge Pin', 'Hinge Pin', '', ( #7210 ) ) ;
#2189=CONICAL_SURFACE ( 'NONE', #6830, 3.400000000000014122, 0.7853981633975372079 ) ;
#2194=VECTOR ( 'NONE', #7487, 1000.000000000000114 ) ;
#2206=ADVANCED_FACE ( 'NONE', ( #126 ), #2189, .T. ) ;
#2238=ORIENTED_EDGE ( 'NONE', *, *, #3036, .T. ) ;
#2255=CARTESIAN_POINT ( 'NONE',  ( -72.90663470102438737, -2.500000000000000444, -375.1168990826883487 ) ) ;
#2299=CARTESIAN_POINT ( 'NONE',  ( -46.74071243416547361, -2.500000000000000000, -414.3237589990478114 ) ) ;
#2311=FACE_OUTER_BOUND ( 'NONE', #7175, .T. ) ;
#2412=( NAMED_UNIT ( * ) PLANE_ANGLE_UNIT ( ) SI_UNIT ( $, .RADIAN. ) );
#2435=CARTESIAN_POINT ( 'NONE',  ( -72.90663470102438737, -2.500000000000000000, -371.7168990826883714 ) ) ;
#2579=VERTEX_POINT ( 'NONE', #6615 ) ;
#2723=EDGE_CURVE ( 'NONE', #2579, #1205, #3601, .T. ) ;
#2817=AXIS2_PLACEMENT_3D ( 'NONE', #8634, #3966, #3161 ) ;
#2827=CONICAL_SURFACE ( 'NONE', #256, 3.400000000000014122, 0.7853981633975631871 ) ;
#3000=( LENGTH_UNIT ( ) NAMED_UNIT ( * ) SI_UNIT ( .MILLI., .METRE. ) );
#3006=FILL_AREA_STYLE ('',( #9361 ) ) ;
#3036=EDGE_CURVE ( 'NONE', #3804, #6040, #6024, .T. ) ;
#3039=DIRECTION ( 'NONE',  ( 0.000000000000000000, -1.000000000000000000, 0.000000000000000000 ) ) ;
#3047=DIRECTION ( 'NONE',  ( 0.000000000000000000, 0.000000000000000000, -1.000000000000000000 ) ) ;
#3104=FILL_AREA_STYLE_COLOUR ( '', #10193 ) ;
#3118=SHAPE_DEFINITION_REPRESENTATION ( #9474, #7381 ) ;
#3135=PRODUCT_DEFINITION_CONTEXT ( 'detailed design', #2153, 'design' ) ;
#3161=DIRECTION ( 'NONE',  ( 1.000000000000000000, 0.000000000000000000, 0.000000000000000000 ) ) ;
#3225=DIRECTION ( 'NONE',  ( 0.000000000000000000, -1.000000000000000000, 0.000000000000000000 ) ) ;
#3267=AXIS2_PLACEMENT_3D ( 'NONE', #8898, #3039, #524 ) ;
#3269=SHAPE_REPRESENTATION_RELATIONSHIP ( 'NONE' , 'NONE' ,  #7381, #8498 ) ;
#3302=AXIS2_PLACEMENT_3D ( 'NONE', #9272, #7008, #3568 ) ;
#3330=VECTOR ( 'NONE', #9820, 1000.000000000000000 ) ;
#3453=CARTESIAN_POINT ( 'NONE',  ( -72.90663470102438737, -12.40000000000001101, -375.2168990826883714 ) ) ;
#3480=DIRECTION ( 'NONE',  ( 0.000000000000000000, 0.000000000000000000, -1.000000000000000000 ) ) ;
#3555=CIRCLE ( 'NONE', #1666, 3.500000000000003109 ) ;
#3568=DIRECTION ( 'NONE',  ( 0.000000000000000000, 0.000000000000000000, -1.000000000000000000 ) ) ;
#3573=CARTESIAN_POINT ( 'NONE',  ( -72.90663470102438737, -12.50000000000000000, -371.7168990826883714 ) ) ;
#3601=LINE ( 'NONE', #6883, #3909 ) ;
#3610=DIRECTION ( 'NONE',  ( 0.000000000000000000, 0.000000000000000000, -1.000000000000000000 ) ) ;
#3629=ORIENTED_EDGE ( 'NONE', *, *, #4360, .F. ) ;
#3760=CIRCLE ( 'NONE', #6162, 3.500000000000003109 ) ;
#3782=AXIS2_PLACEMENT_3D ( 'NONE', #1675, #861, #813 ) ;
#3804=VERTEX_POINT ( 'NONE', #9187 ) ;
#3811=SURFACE_STYLE_FILL_AREA ( #3006 ) ;
#3838=( GEOMETRIC_REPRESENTATION_CONTEXT ( 3 ) GLOBAL_UNCERTAINTY_ASSIGNED_CONTEXT ( ( #1844 ) ) GLOBAL_UNIT_ASSIGNED_CONTEXT ( ( #3000, #6380, #9608 ) ) REPRESENTATION_CONTEXT ( 'NONE', 'WORKASPACE' ) );
#3849=( GEOMETRIC_REPRESENTATION_CONTEXT ( 3 ) GLOBAL_UNCERTAINTY_ASSIGNED_CONTEXT ( ( #7536 ) ) GLOBAL_UNIT_ASSIGNED_CONTEXT ( ( #4615, #430, #10154 ) ) REPRESENTATION_CONTEXT ( 'NONE', 'WORKASPACE' ) );
#3904=ORIENTED_EDGE ( 'NONE', *, *, #10269, .F. ) ;
#3909=VECTOR ( 'NONE', #5305, 1000.000000000000000 ) ;
#3966=DIRECTION ( 'NONE',  ( 0.000000000000000000, 0.000000000000000000, 1.000000000000000000 ) ) ;
#4019=AXIS2_PLACEMENT_3D ( 'NONE', #225, #4359, #5160 ) ;
#4114=DIRECTION ( 'NONE',  ( 0.000000000000000000, -1.000000000000000000, 0.000000000000000000 ) ) ;
#4317=UNCERTAINTY_MEASURE_WITH_UNIT (LENGTH_MEASURE( 1.000000000000000082E-05 ), #1657, 'distance_accuracy_value', 'NONE');
#4359=DIRECTION ( 'NONE',  ( 0.000000000000000000, 1.000000000000000000, 0.000000000000000000 ) ) ;
#4360=EDGE_CURVE ( 'NONE', #5864, #1205, #1715, .T. ) ;
#4476=ORIENTED_EDGE ( 'NONE', *, *, #2723, .F. ) ;
#4483=CARTESIAN_POINT ( 'NONE',  ( -72.90663470102438737, -12.50000000000000000, -368.3168990826883373 ) ) ;
#4595=DIRECTION ( 'NONE',  ( 0.000000000000000000, -1.000000000000000000, 0.000000000000000000 ) ) ;
#4615=( LENGTH_UNIT ( ) NAMED_UNIT ( * ) SI_UNIT ( .MILLI., .METRE. ) );
#4706=ADVANCED_FACE ( 'NONE', ( #1857 ), #1910, .T. ) ;
#4748=EDGE_LOOP ( 'NONE', ( #3629, #9256, #1292, #8710 ) ) ;
#4774=FACE_OUTER_BOUND ( 'NONE', #8383, .T. ) ;
#4778=SURFACE_STYLE_USAGE ( .BOTH. , #1498 ) ;
#4813=VERTEX_POINT ( 'NONE', #6340 ) ;
#4828=DIRECTION ( 'NONE',  ( -0.8820010751365675583, 0.000000000000000000, -0.4712473909295827323 ) ) ;
#4877=CARTESIAN_POINT ( 'NONE',  ( -72.90663470102438737, -12.50000000000000000, -368.3168990826883373 ) ) ;
#4888=CARTESIAN_POINT ( 'NONE',  ( -72.90663470102438737, -12.50000000000000000, -375.1168990826883487 ) ) ;
#4987=CARTESIAN_POINT ( 'NONE',  ( -72.90663470102438737, -12.50000000000000000, -375.1168990826883487 ) ) ;
#5000=FACE_OUTER_BOUND ( 'NONE', #9726, .T. ) ;
#5027=DIRECTION ( 'NONE',  ( 0.000000000000000000, -1.000000000000000000, 0.000000000000000000 ) ) ;
#5126=DIRECTION ( 'NONE',  ( 0.000000000000000000, -0.000000000000000000, -1.000000000000000000 ) ) ;
#5154=AXIS2_PLACEMENT_3D ( 'NONE', #2299, #9822, #4828 ) ;
#5160=DIRECTION ( 'NONE',  ( 0.000000000000000000, 0.000000000000000000, -1.000000000000000000 ) ) ;
#5216=DIRECTION ( 'NONE',  ( 0.000000000000000000, 1.000000000000000000, 0.000000000000000000 ) ) ;
#5229=CONICAL_SURFACE ( 'NONE', #603, 3.400000000000014122, 0.7853981633975631871 ) ;
#5242=CYLINDRICAL_SURFACE ( 'NONE', #1618, 3.500000000000003109 ) ;
#5289=DIRECTION ( 'NONE',  ( 0.000000000000000000, 0.000000000000000000, -1.000000000000000000 ) ) ;
#5305=DIRECTION ( 'NONE',  ( 0.000000000000000000, -1.000000000000000000, 0.000000000000000000 ) ) ;
#5381=MECHANICAL_DESIGN_GEOMETRIC_PRESENTATION_REPRESENTATION('',(#8640),#3849);
#5494=ORIENTED_EDGE ( 'NONE', *, *, #10149, .F. ) ;
#5555=FACE_OUTER_BOUND ( 'NONE', #9323, .T. ) ;
#5557=CIRCLE ( 'NONE', #4019, 3.500000000000003109 ) ;
#5574=SURFACE_STYLE_FILL_AREA ( #9661 ) ;
#5581=CYLINDRICAL_SURFACE ( 'NONE', #7245, 3.500000000000003109 ) ;
#5602=DIRECTION ( 'NONE',  ( 0.000000000000000000, 0.000000000000000000, -1.000000000000000000 ) ) ;
#5643=FACE_OUTER_BOUND ( 'NONE', #4748, .T. ) ;
#5686=DIRECTION ( 'NONE',  ( 0.000000000000000000, 0.000000000000000000, -1.000000000000000000 ) ) ;
#5705=DIRECTION ( 'NONE',  ( 0.000000000000000000, 0.000000000000000000, -1.000000000000000000 ) ) ;
#5706=EDGE_CURVE ( 'NONE', #8252, #2579, #10523, .T. ) ;
#5864=VERTEX_POINT ( 'NONE', #4888 ) ;
#5871=ADVANCED_FACE ( 'NONE', ( #2311 ), #5581, .T. ) ;
#6024=LINE ( 'NONE', #10163, #2194 ) ;
#6027=ORIENTED_EDGE ( 'NONE', *, *, #8297, .T. ) ;
#6040=VERTEX_POINT ( 'NONE', #9349 ) ;
#6162=AXIS2_PLACEMENT_3D ( 'NONE', #8938, #6410, #5602 ) ;
#6281=SURFACE_SIDE_STYLE ('',( #3811 ) ) ;
#6318=PLANE ( 'NONE',  #5154 ) ;
#6340=CARTESIAN_POINT ( 'NONE',  ( -72.90663470102438737, -12.40000000000001101, -368.2168990826883146 ) ) ;
#6351=ORIENTED_EDGE ( 'NONE', *, *, #9742, .T. ) ;
#6380=( NAMED_UNIT ( * ) PLANE_ANGLE_UNIT ( ) SI_UNIT ( $, .RADIAN. ) );
#6382=CARTESIAN_POINT ( 'NONE',  ( -72.90663470102438737, -2.500000000000000000, -375.1168990826883487 ) ) ;
#6410=DIRECTION ( 'NONE',  ( 0.000000000000000000, 1.000000000000000000, 0.000000000000000000 ) ) ;
#6430=ORIENTED_EDGE ( 'NONE', *, *, #3036, .F. ) ;
#6487=EDGE_LOOP ( 'NONE', ( #9108, #8131, #9080, #5494 ) ) ;
#6547=EDGE_CURVE ( 'NONE', #8252, #3804, #9475, .T. ) ;
#6599=COLOUR_RGB ( '', 0.31764706, 0.68627451, 0.89019608) ;
#6615=CARTESIAN_POINT ( 'NONE',  ( -72.90663470102438737, -2.599999999999984102, -375.2168990826883714 ) ) ;
#6764=AXIS2_PLACEMENT_3D ( 'NONE', #9123, #5027, #3480 ) ;
#6830=AXIS2_PLACEMENT_3D ( 'NONE', #920, #5216, #8493 ) ;
#6883=CARTESIAN_POINT ( 'NONE',  ( -72.90663470102438737, 7.399494936611693774, -375.2168990826883714 ) ) ;
#6938=STYLED_ITEM ( 'NONE', ( #7247 ), #8498 ) ;
#6970=ORIENTED_EDGE ( 'NONE', *, *, #5706, .F. ) ;
#7008=DIRECTION ( 'NONE',  ( -0.000000000000000000, 1.000000000000000000, -0.000000000000000000 ) ) ;
#7025=ADVANCED_FACE ( 'NONE', ( #4774 ), #6318, .F. ) ;
#7077=EDGE_CURVE ( 'NONE', #5864, #10381, #1379, .T. ) ;
#7105=( GEOMETRIC_REPRESENTATION_CONTEXT ( 3 ) GLOBAL_UNCERTAINTY_ASSIGNED_CONTEXT ( ( #4317 ) ) GLOBAL_UNIT_ASSIGNED_CONTEXT ( ( #1657, #2412, #1609 ) ) REPRESENTATION_CONTEXT ( 'NONE', 'WORKASPACE' ) );
#7119=VECTOR ( 'NONE', #352, 1000.000000000000000 ) ;
#7175=EDGE_LOOP ( 'NONE', ( #2066, #6351, #1836, #4476 ) ) ;
#7210=PRODUCT_CONTEXT ( 'NONE', #14, 'mechanical' ) ;
#7237=ORIENTED_EDGE ( 'NONE', *, *, #1252, .T. ) ;
#7245=AXIS2_PLACEMENT_3D ( 'NONE', #1505, #3225, #5686 ) ;
#7247=PRESENTATION_STYLE_ASSIGNMENT (( #4778 ) ) ;
#7287=CARTESIAN_POINT ( 'NONE',  ( -72.90663470102438737, -2.500000000000000444, -371.7168990826883714 ) ) ;
#7326=DIRECTION ( 'NONE',  ( -0.000000000000000000, 1.000000000000000000, -0.000000000000000000 ) ) ;
#7369=AXIS2_PLACEMENT_3D ( 'NONE', #2435, #7326, #5705 ) ;
#7381=SHAPE_REPRESENTATION ( 'Hinge Pin', ( #2817 ), #3838 ) ;
#7387=ORIENTED_EDGE ( 'NONE', *, *, #7077, .T. ) ;
#7420=ORIENTED_EDGE ( 'NONE', *, *, #5706, .T. ) ;
#7471=EDGE_CURVE ( 'NONE', #4813, #1205, #3760, .T. ) ;
#7487=DIRECTION ( 'NONE',  ( 8.659560562355927562E-17, -0.7071067811864661934, 0.7071067811866287300 ) ) ;
#7536=UNCERTAINTY_MEASURE_WITH_UNIT (LENGTH_MEASURE( 1.000000000000000082E-05 ), #4615, 'distance_accuracy_value', 'NONE');
#7762=FACE_OUTER_BOUND ( 'NONE', #8510, .T. ) ;
#7811=LINE ( 'NONE', #2018, #7119 ) ;
#7818=PRODUCT_DEFINITION_FORMATION_WITH_SPECIFIED_SOURCE ( 'ANY', '', #2183, .NOT_KNOWN. ) ;
#8131=ORIENTED_EDGE ( 'NONE', *, *, #4360, .T. ) ;
#8252=VERTEX_POINT ( 'NONE', #6382 ) ;
#8297=EDGE_CURVE ( 'NONE', #10381, #5864, #1369, .T. ) ;
#8337=DIRECTION ( 'NONE',  ( 0.000000000000000000, 0.000000000000000000, -1.000000000000000000 ) ) ;
#8383=EDGE_LOOP ( 'NONE', ( #985, #593 ) ) ;
#8421=DIRECTION ( 'NONE',  ( 8.659560562355704463E-17, 0.7071067811864846231, -0.7071067811866105224 ) ) ;
#8493=DIRECTION ( 'NONE',  ( 0.000000000000000000, 0.000000000000000000, 1.000000000000000000 ) ) ;
#8498=ADVANCED_BREP_SHAPE_REPRESENTATION ( '', ( #8977, #2817 ), #3838 ) ;
#8510=EDGE_LOOP ( 'NONE', ( #54, #7237, #9334, #491 ) ) ;
#8634=CARTESIAN_POINT ( 'NONE',  ( 0.000000000000000000, 0.000000000000000000, 0.000000000000000000 ) ) ;
#8640=STYLED_ITEM ( 'NONE', ( #2043 ), #8977 ) ;
#8710=ORIENTED_EDGE ( 'NONE', *, *, #8849, .F. ) ;
#8755=CONICAL_SURFACE ( 'NONE', #3782, 3.400000000000014122, 0.7853981633975372079 ) ;
#8849=EDGE_CURVE ( 'NONE', #1205, #4813, #5557, .T. ) ;
#8885=PRODUCT_DEFINITION ( 'UNKNOWN', '', #7818, #3135 ) ;
#8898=CARTESIAN_POINT ( 'NONE',  ( -72.90663470102438737, -12.50000000000000000, -371.7168990826883714 ) ) ;
#8938=CARTESIAN_POINT ( 'NONE',  ( -72.90663470102438737, -12.40000000000001101, -371.7168990826883714 ) ) ;
#8953=ORIENTED_EDGE ( 'NONE', *, *, #693, .F. ) ;
#8977=MANIFOLD_SOLID_BREP ( 'Stock-MAS-686-1', #9865 ) ;
#8989=DIRECTION ( 'NONE',  ( 0.000000000000000000, -1.000000000000000000, 0.000000000000000000 ) ) ;
#9008=AXIS2_PLACEMENT_3D ( 'NONE', #3573, #10176, #5126 ) ;
#9080=ORIENTED_EDGE ( 'NONE', *, *, #7471, .F. ) ;
#9108=ORIENTED_EDGE ( 'NONE', *, *, #7077, .F. ) ;
#9123=CARTESIAN_POINT ( 'NONE',  ( -72.90663470102438737, -2.599999999999984102, -371.7168990826883714 ) ) ;
#9187=CARTESIAN_POINT ( 'NONE',  ( -72.90663470102438737, -2.500000000000000000, -368.3168990826883373 ) ) ;
#9256=ORIENTED_EDGE ( 'NONE', *, *, #8297, .F. ) ;
#9272=CARTESIAN_POINT ( 'NONE',  ( -72.90663470102438737, -2.500000000000000000, -371.7168990826883714 ) ) ;
#9323=EDGE_LOOP ( 'NONE', ( #8953, #2238, #3904, #6970 ) ) ;
#9334=ORIENTED_EDGE ( 'NONE', *, *, #2723, .T. ) ;
#9349=CARTESIAN_POINT ( 'NONE',  ( -72.90663470102438737, -2.599999999999984102, -368.2168990826883146 ) ) ;
#9361=FILL_AREA_STYLE_COLOUR ( '', #6599 ) ;
#9433=ORIENTED_EDGE ( 'NONE', *, *, #1252, .F. ) ;
#9474=PRODUCT_DEFINITION_SHAPE ( 'NONE', 'NONE',  #8885 ) ;
#9475=CIRCLE ( 'NONE', #3302, 3.400000000000014122 ) ;
#9594=CIRCLE ( 'NONE', #7369, 3.400000000000014122 ) ;
#9603=DIRECTION ( 'NONE',  ( 0.000000000000000000, -1.000000000000000000, 0.000000000000000000 ) ) ;
#9608=( NAMED_UNIT ( * ) SI_UNIT ( $, .STERADIAN. ) SOLID_ANGLE_UNIT ( ) );
#9619=AXIS2_PLACEMENT_3D ( 'NONE', #10459, #9603, #3047 ) ;
#9661=FILL_AREA_STYLE ('',( #3104 ) ) ;
#9726=EDGE_LOOP ( 'NONE', ( #6430, #873, #7420, #9433 ) ) ;
#9742=EDGE_CURVE ( 'NONE', #6040, #4813, #7811, .T. ) ;
#9820=DIRECTION ( 'NONE',  ( 0.000000000000000000, 0.7071067811864846231, 0.7071067811866105224 ) ) ;
#9822=DIRECTION ( 'NONE',  ( 0.000000000000000000, -1.000000000000000000, -0.000000000000000000 ) ) ;
#9837=VECTOR ( 'NONE', #8421, 1000.000000000000000 ) ;
#9865=CLOSED_SHELL ( 'NONE', ( #353, #2206, #5871, #10389, #4706, #7025, #1812, #101 ) ) ;
#10062=CARTESIAN_POINT ( 'NONE',  ( -72.90663470102438737, -2.599999999999984102, -371.7168990826883714 ) ) ;
#10149=EDGE_CURVE ( 'NONE', #10381, #4813, #1605, .T. ) ;
#10154=( NAMED_UNIT ( * ) SI_UNIT ( $, .STERADIAN. ) SOLID_ANGLE_UNIT ( ) );
#10163=CARTESIAN_POINT ( 'NONE',  ( -72.90663470102438737, -2.500000000000000444, -368.3168990826883373 ) ) ;
#10176=DIRECTION ( 'NONE',  ( 0.000000000000000000, -1.000000000000000000, 0.000000000000000000 ) ) ;
#10193=COLOUR_RGB ( '', 0.31764706, 0.68627451, 0.89019608) ;
#10269=EDGE_CURVE ( 'NONE', #2579, #6040, #1256, .T. ) ;
#10381=VERTEX_POINT ( 'NONE', #4483 ) ;
#10389=ADVANCED_FACE ( 'NONE', ( #7762 ), #5242, .T. ) ;
#10459=CARTESIAN_POINT ( 'NONE',  ( -72.90663470102438737, -12.50000000000000000, -371.7168990826883714 ) ) ;
#10523=LINE ( 'NONE', #2255, #2088 ) ;
ENDSEC;
END-ISO-10303-21;
